ISO-10303-21;
HEADER;
FILE_DESCRIPTION (('STEP AP214'),
    '1' );
FILE_NAME ('rubber for drip tip.step',
    '2026-10-05T20:10:51',
    ( '' ),
    ( '' ),
    'SwSTEP 2.0',
    'SolidWorks 2020',
    '' );
FILE_SCHEMA (( 'AUTOMOTIVE_DESIGN' ));
ENDSEC;

DATA;
#482=ORIENTED_EDGE ( 'NONE', *, *, #180142, .T. ) ;
#666=CARTESIAN_POINT ( 'NONE',  ( 0.000000000000000000, 0.6185895741317448682, 0.000000000000000000 ) ) ;
#2407=CIRCLE ( 'NONE', #109821, 6.264285714285709794 ) ;
#2669=UNCERTAINTY_MEASURE_WITH_UNIT (LENGTH_MEASURE( 1.000000000000000082E-05 ), #201758, 'distance_accuracy_value', 'NONE');
#2966=AXIS2_PLACEMENT_3D ( 'NONE', #78648, #112296, #209704 ) ;
#3337=EDGE_CURVE ( 'NONE', #95100, #171070, #193035, .T. ) ;
#4333=ORIENTED_EDGE ( 'NONE', *, *, #126049, .T. ) ;
#4511=( NAMED_UNIT ( * ) SI_UNIT ( $, .STERADIAN. ) SOLID_ANGLE_UNIT ( ) );
#5851=ORIENTED_EDGE ( 'NONE', *, *, #91556, .F. ) ;
#5948=CARTESIAN_POINT ( 'NONE',  ( 0.000000000000000000, 0.4330127018922214077, 0.000000000000000000 ) ) ;
#7081=( GEOMETRIC_REPRESENTATION_CONTEXT ( 3 ) GLOBAL_UNCERTAINTY_ASSIGNED_CONTEXT ( ( #11863 ) ) GLOBAL_UNIT_ASSIGNED_CONTEXT ( ( #8814, #105274, #4511 ) ) REPRESENTATION_CONTEXT ( 'NONE', 'WORKASPACE' ) );
#7337=ORIENTED_EDGE ( 'NONE', *, *, #129965, .T. ) ;
#8222=AXIS2_PLACEMENT_3D ( 'NONE', #178795, #80206, #210196 ) ;
#8787=ORIENTED_EDGE ( 'NONE', *, *, #101370, .F. ) ;
#8814=( LENGTH_UNIT ( ) NAMED_UNIT ( * ) SI_UNIT ( .MILLI., .METRE. ) );
#9052=ORIENTED_EDGE ( 'NONE', *, *, #21416, .F. ) ;
#9329=AXIS2_PLACEMENT_3D ( 'NONE', #5948, #104562, #101340 ) ;
#9916=DIRECTION ( 'NONE',  ( 0.000000000000000000, 0.000000000000000000, 1.000000000000000000 ) ) ;
#11863=UNCERTAINTY_MEASURE_WITH_UNIT (LENGTH_MEASURE( 1.000000000000000082E-05 ), #8814, 'distance_accuracy_value', 'NONE');
#12000=CARTESIAN_POINT ( 'NONE',  ( 0.000000000000000000, -0.4330127018922214077, 0.000000000000000000 ) ) ;
#12599=ORIENTED_EDGE ( 'NONE', *, *, #203560, .T. ) ;
#14293=CARTESIAN_POINT ( 'NONE',  ( 4.296393142825893463, 0.4330127018922214077, -4.470011852588159584 ) ) ;
#14858=AXIS2_PLACEMENT_3D ( 'NONE', #156926, #206714, #58342 ) ;
#15428=ORIENTED_EDGE ( 'NONE', *, *, #203560, .F. ) ;
#16236=VERTEX_POINT ( 'NONE', #100143 ) ;
#17535=CARTESIAN_POINT ( 'NONE',  ( 4.296393142825893463, -0.4330127018922214077, -4.470011852588159584 ) ) ;
#17857=UNCERTAINTY_MEASURE_WITH_UNIT (LENGTH_MEASURE( 1.000000000000000082E-05 ), #202827, 'distance_accuracy_value', 'NONE');
#19259=EDGE_CURVE ( 'NONE', #23806, #16236, #47544, .T. ) ;
#19509=DIRECTION ( 'NONE',  ( 0.000000000000000000, 0.000000000000000000, -1.000000000000000000 ) ) ;
#21416=EDGE_CURVE ( 'NONE', #33049, #95100, #189819, .T. ) ;
#21828=SURFACE_STYLE_FILL_AREA ( #121586 ) ;
#23806=VERTEX_POINT ( 'NONE', #14293 ) ;
#24371=CARTESIAN_POINT ( 'NONE',  ( 0.000000000000000000, 0.6185895741317448682, 6.264285714285709794 ) ) ;
#25163=SHAPE_REPRESENTATION_RELATIONSHIP ( 'NONE' , 'NONE' ,  #62426, #181761 ) ;
#25640=DIRECTION ( 'NONE',  ( -1.000000000000000000, 0.000000000000000000, 0.000000000000000000 ) ) ;
#25799=ORIENTED_EDGE ( 'NONE', *, *, #75497, .T. ) ;
#26764=EDGE_LOOP ( 'NONE', ( #482, #82600, #143384, #88275 ) ) ;
#28299=MECHANICAL_DESIGN_GEOMETRIC_PRESENTATION_REPRESENTATION('',(#38659),#7081);
#29241=AXIS2_PLACEMENT_3D ( 'NONE', #48246, #115416, #95932 ) ;
#29319=EDGE_LOOP ( 'NONE', ( #125613, #173002, #7337, #106352, #189033, #114658 ) ) ;
#29872=EDGE_LOOP ( 'NONE', ( #8787, #197268, #30381, #53624, #5851 ) ) ;
#30083=DIRECTION ( 'NONE',  ( -1.000000000000000000, 0.000000000000000000, 0.000000000000000000 ) ) ;
#30381=ORIENTED_EDGE ( 'NONE', *, *, #19259, .F. ) ;
#31150=COLOUR_RGB ( '', 0.31764706, 0.68627451, 0.89019608) ;
#31610=CIRCLE ( 'NONE', #100851, 1.000000000000000000 ) ;
#32785=EDGE_CURVE ( 'NONE', #171070, #130050, #168293, .T. ) ;
#32954=EDGE_LOOP ( 'NONE', ( #9052, #15428, #25799, #91825, #131115 ) ) ;
#33049=VERTEX_POINT ( 'NONE', #66235 ) ;
#33425=ADVANCED_FACE ( 'NONE', ( #166984 ), #196687, .T. ) ;
#33721=DIRECTION ( 'NONE',  ( 1.000000000000000000, 0.000000000000000000, -1.224646799147353207E-16 ) ) ;
#34115=AXIS2_PLACEMENT_3D ( 'NONE', #179989, #33721, #147496 ) ;
#37146=( NAMED_UNIT ( * ) PLANE_ANGLE_UNIT ( ) SI_UNIT ( $, .RADIAN. ) );
#37537=ORIENTED_EDGE ( 'NONE', *, *, #178413, .T. ) ;
#38290=DIRECTION ( 'NONE',  ( 0.000000000000000000, 1.000000000000000000, 0.000000000000000000 ) ) ;
#38293=CARTESIAN_POINT ( 'NONE',  ( 0.000000000000000000, -0.4330127018922214077, -6.200000000000000178 ) ) ;
#38659=STYLED_ITEM ( 'NONE', ( #205943 ), #167773 ) ;
#40378=CARTESIAN_POINT ( 'NONE',  ( 0.000000000000000000, 0.000000000000000000, 0.000000000000000000 ) ) ;
#40935=VERTEX_POINT ( 'NONE', #151814 ) ;
#41063=EDGE_LOOP ( 'NONE', ( #51662, #140408, #190802, #202507, #208213 ) ) ;
#41286=CARTESIAN_POINT ( 'NONE',  ( 0.000000000000000000, 0.4330127018922214077, 0.000000000000000000 ) ) ;
#42700=DIRECTION ( 'NONE',  ( 0.000000000000000000, 0.000000000000000000, -1.000000000000000000 ) ) ;
#43139=CIRCLE ( 'NONE', #188424, 6.264285714285709794 ) ;
#45456=DIRECTION ( 'NONE',  ( 1.224646799147353454E-16, 0.000000000000000000, -1.000000000000000000 ) ) ;
#47544=CIRCLE ( 'NONE', #9329, 6.200000000000000178 ) ;
#47772=CARTESIAN_POINT ( 'NONE',  ( 0.000000000000000000, -0.6185895741317448682, 0.000000000000000000 ) ) ;
#47900=AXIS2_PLACEMENT_3D ( 'NONE', #140772, #207850, #125633 ) ;
#48246=CARTESIAN_POINT ( 'NONE',  ( 0.000000000000000000, -0.4330127018922214077, 0.000000000000000000 ) ) ;
#49964=VERTEX_POINT ( 'NONE', #17535 ) ;
#51662=ORIENTED_EDGE ( 'NONE', *, *, #180142, .F. ) ;
#53624=ORIENTED_EDGE ( 'NONE', *, *, #126049, .F. ) ;
#55359=EDGE_CURVE ( 'NONE', #112763, #40935, #163645, .T. ) ;
#55541=( NAMED_UNIT ( * ) SI_UNIT ( $, .STERADIAN. ) SOLID_ANGLE_UNIT ( ) );
#56380=VERTEX_POINT ( 'NONE', #38293 ) ;
#56612=SURFACE_SIDE_STYLE ('',( #121695 ) ) ;
#56908=DIRECTION ( 'NONE',  ( -1.000000000000000000, -0.000000000000000000, -0.000000000000000000 ) ) ;
#58342=DIRECTION ( 'NONE',  ( 0.000000000000000000, 0.000000000000000000, 1.000000000000000000 ) ) ;
#58459=DIRECTION ( 'NONE',  ( 1.224646799147353207E-16, 0.000000000000000000, -1.000000000000000000 ) ) ;
#58814=STYLED_ITEM ( 'NONE', ( #169287 ), #181761 ) ;
#58896=APPLICATION_CONTEXT ( 'automotive_design' ) ;
#60090=EDGE_CURVE ( 'NONE', #138365, #40935, #31610, .T. ) ;
#60436=ORIENTED_EDGE ( 'NONE', *, *, #64698, .F. ) ;
#61008=AXIS2_PLACEMENT_3D ( 'NONE', #41286, #75891, #106312 ) ;
#61832=DIRECTION ( 'NONE',  ( 0.000000000000000000, -1.000000000000000000, 0.000000000000000000 ) ) ;
#62426=SHAPE_REPRESENTATION ( 'rubber for drip tip', ( #200407 ), #124768 ) ;
#62470=EDGE_LOOP ( 'NONE', ( #110779, #120571, #122925, #157467, #66735, #4333 ) ) ;
#64521=PRODUCT_DEFINITION_SHAPE ( 'NONE', 'NONE',  #173573 ) ;
#64698=EDGE_CURVE ( 'NONE', #16236, #130050, #122120, .T. ) ;
#64970=DIRECTION ( 'NONE',  ( 0.000000000000000000, 1.000000000000000000, 0.000000000000000000 ) ) ;
#65071=EDGE_CURVE ( 'NONE', #56380, #49964, #87561, .T. ) ;
#65941=DIRECTION ( 'NONE',  ( 0.000000000000000000, 0.000000000000000000, -1.000000000000000000 ) ) ;
#66114=LINE ( 'NONE', #166857, #104816 ) ;
#66235=CARTESIAN_POINT ( 'NONE',  ( 0.000000000000000000, -0.6185895741317448682, 6.264285714285709794 ) ) ;
#66735=ORIENTED_EDGE ( 'NONE', *, *, #214139, .T. ) ;
#67150=DIRECTION ( 'NONE',  ( 0.000000000000000000, 1.000000000000000000, 0.000000000000000000 ) ) ;
#67186=CARTESIAN_POINT ( 'NONE',  ( -4.296393142825893463, 0.4330127018922214077, 4.470011852588161361 ) ) ;
#67800=DIRECTION ( 'NONE',  ( 0.000000000000000000, 0.000000000000000000, -1.000000000000000000 ) ) ;
#68252=DIRECTION ( 'NONE',  ( 0.000000000000000000, 0.000000000000000000, 1.000000000000000000 ) ) ;
#68765=CARTESIAN_POINT ( 'NONE',  ( 7.671537448944488015E-16, -0.6185895741317448682, -6.264285714285709794 ) ) ;
#69443=DIRECTION ( 'NONE',  ( 0.000000000000000000, 1.000000000000000000, 0.000000000000000000 ) ) ;
#69786=ADVANCED_FACE ( 'NONE', ( #213382 ), #195008, .T. ) ;
#69800=ADVANCED_FACE ( 'NONE', ( #161483 ), #129384, .T. ) ;
#70906=AXIS2_PLACEMENT_3D ( 'NONE', #77759, #30083, #96175 ) ;
#75175=CARTESIAN_POINT ( 'NONE',  ( 0.000000000000000000, -0.4330127018922214077, 0.000000000000000000 ) ) ;
#75497=EDGE_CURVE ( 'NONE', #138365, #56380, #180547, .T. ) ;
#75804=CARTESIAN_POINT ( 'NONE',  ( 8.633759933988839975E-16, 0.000000000000000000, -7.049999999999999822 ) ) ;
#75891=DIRECTION ( 'NONE',  ( 0.000000000000000000, 1.000000000000000000, 0.000000000000000000 ) ) ;
#77233=VECTOR ( 'NONE', #38290, 1000.000000000000000 ) ;
#77759=CARTESIAN_POINT ( 'NONE',  ( 0.000000000000000000, 0.4330127018922214077, 6.500000000000000000 ) ) ;
#78075=DIRECTION ( 'NONE',  ( 0.000000000000000000, 0.000000000000000000, -1.000000000000000000 ) ) ;
#78648=CARTESIAN_POINT ( 'NONE',  ( 0.000000000000000000, -2.000000000000001776, 0.000000000000000000 ) ) ;
#79500=ADVANCED_FACE ( 'NONE', ( #111679 ), #211224, .F. ) ;
#79719=CYLINDRICAL_SURFACE ( 'NONE', #2966, 6.200000000000000178 ) ;
#80206=DIRECTION ( 'NONE',  ( 0.000000000000000000, 1.000000000000000000, 0.000000000000000000 ) ) ;
#81445=ADVANCED_FACE ( 'NONE', ( #193321 ), #194748, .T. ) ;
#82600=ORIENTED_EDGE ( 'NONE', *, *, #60090, .T. ) ;
#84018=SHAPE_DEFINITION_REPRESENTATION ( #64521, #62426 ) ;
#85265=CIRCLE ( 'NONE', #61008, 6.200000000000000178 ) ;
#85539=ADVANCED_FACE ( 'NONE', ( #206048 ), #152561, .T. ) ;
#85907=CARTESIAN_POINT ( 'NONE',  ( 0.000000000000000000, -0.4330127018922214077, 0.000000000000000000 ) ) ;
#86487=MECHANICAL_DESIGN_GEOMETRIC_PRESENTATION_REPRESENTATION('',(#58814),#107581);
#87051=COLOUR_RGB ( '', 0.31764706, 0.68627451, 0.89019608) ;
#87561=CIRCLE ( 'NONE', #104729, 6.200000000000000178 ) ;
#87928=CIRCLE ( 'NONE', #108714, 0.2999999999999999334 ) ;
#87936=SURFACE_STYLE_USAGE ( .BOTH. , #137770 ) ;
#88275=ORIENTED_EDGE ( 'NONE', *, *, #178413, .F. ) ;
#90914=TOROIDAL_SURFACE ( 'NONE', #118631, 7.049999999999999822, 0.9999999999999997780 ) ;
#91556=EDGE_CURVE ( 'NONE', #112763, #176746, #143667, .T. ) ;
#91825=ORIENTED_EDGE ( 'NONE', *, *, #156316, .F. ) ;
#92398=EDGE_LOOP ( 'NONE', ( #195041, #12599, #37537, #190804 ) ) ;
#92967=AXIS2_PLACEMENT_3D ( 'NONE', #137687, #69443, #200513 ) ;
#93972=ORIENTED_EDGE ( 'NONE', *, *, #116150, .F. ) ;
#95100=VERTEX_POINT ( 'NONE', #125044 ) ;
#95216=CARTESIAN_POINT ( 'NONE',  ( 0.000000000000000000, 0.000000000000000000, 0.000000000000000000 ) ) ;
#95645=ORIENTED_EDGE ( 'NONE', *, *, #214139, .F. ) ;
#95932=DIRECTION ( 'NONE',  ( 0.000000000000000000, 0.000000000000000000, -1.000000000000000000 ) ) ;
#96175=DIRECTION ( 'NONE',  ( 0.000000000000000000, 0.000000000000000000, 1.000000000000000000 ) ) ;
#97515=APPLICATION_CONTEXT ( 'automotive_design' ) ;
#98035=AXIS2_PLACEMENT_3D ( 'NONE', #139423, #25640, #175126 ) ;
#100143=CARTESIAN_POINT ( 'NONE',  ( 7.632173801829039911E-16, 0.4330127018922214077, -6.200000000000000178 ) ) ;
#100851=AXIS2_PLACEMENT_3D ( 'NONE', #75804, #195963, #45456 ) ;
#101340=DIRECTION ( 'NONE',  ( 0.000000000000000000, 0.000000000000000000, 1.000000000000000000 ) ) ;
#101370=EDGE_CURVE ( 'NONE', #40935, #112763, #2407, .T. ) ;
#104298=FILL_AREA_STYLE_COLOUR ( '', #31150 ) ;
#104300=DIRECTION ( 'NONE',  ( 0.000000000000000000, 0.000000000000000000, 1.000000000000000000 ) ) ;
#104562=DIRECTION ( 'NONE',  ( 0.000000000000000000, 1.000000000000000000, 0.000000000000000000 ) ) ;
#104729=AXIS2_PLACEMENT_3D ( 'NONE', #199319, #116023, #19509 ) ;
#104816=VECTOR ( 'NONE', #120308, 1000.000000000000000 ) ;
#105274=( NAMED_UNIT ( * ) PLANE_ANGLE_UNIT ( ) SI_UNIT ( $, .RADIAN. ) );
#106312=DIRECTION ( 'NONE',  ( 0.000000000000000000, 0.000000000000000000, 1.000000000000000000 ) ) ;
#106352=ORIENTED_EDGE ( 'NONE', *, *, #19259, .T. ) ;
#107581=( GEOMETRIC_REPRESENTATION_CONTEXT ( 3 ) GLOBAL_UNCERTAINTY_ASSIGNED_CONTEXT ( ( #17857 ) ) GLOBAL_UNIT_ASSIGNED_CONTEXT ( ( #202827, #189799, #155182 ) ) REPRESENTATION_CONTEXT ( 'NONE', 'WORKASPACE' ) );
#107729=PRODUCT_DEFINITION_FORMATION_WITH_SPECIFIED_SOURCE ( 'ANY', '', #157772, .NOT_KNOWN. ) ;
#107875=ORIENTED_EDGE ( 'NONE', *, *, #55359, .F. ) ;
#108714=AXIS2_PLACEMENT_3D ( 'NONE', #206825, #207890, #58459 ) ;
#109638=CARTESIAN_POINT ( 'NONE',  ( 0.000000000000000000, 0.000000000000000000, 0.000000000000000000 ) ) ;
#109821=AXIS2_PLACEMENT_3D ( 'NONE', #111887, #124946, #65941 ) ;
#109876=DIRECTION ( 'NONE',  ( 0.000000000000000000, -1.000000000000000000, 0.000000000000000000 ) ) ;
#110779=ORIENTED_EDGE ( 'NONE', *, *, #129965, .F. ) ;
#111679=FACE_OUTER_BOUND ( 'NONE', #29319, .T. ) ;
#111887=CARTESIAN_POINT ( 'NONE',  ( 0.000000000000000000, 0.6185895741317448682, 0.000000000000000000 ) ) ;
#112296=DIRECTION ( 'NONE',  ( 0.000000000000000000, 1.000000000000000000, 0.000000000000000000 ) ) ;
#112763=VERTEX_POINT ( 'NONE', #24371 ) ;
#114658=ORIENTED_EDGE ( 'NONE', *, *, #32785, .F. ) ;
#115416=DIRECTION ( 'NONE',  ( 0.000000000000000000, -1.000000000000000000, 0.000000000000000000 ) ) ;
#116023=DIRECTION ( 'NONE',  ( 0.000000000000000000, -1.000000000000000000, 0.000000000000000000 ) ) ;
#116150=EDGE_CURVE ( 'NONE', #40935, #16236, #87928, .T. ) ;
#118631=AXIS2_PLACEMENT_3D ( 'NONE', #109638, #207045, #9916 ) ;
#118783=DIRECTION ( 'NONE',  ( 0.000000000000000000, -1.000000000000000000, 0.000000000000000000 ) ) ;
#120308=DIRECTION ( 'NONE',  ( 0.000000000000000000, 1.000000000000000000, 0.000000000000000000 ) ) ;
#120571=ORIENTED_EDGE ( 'NONE', *, *, #181980, .T. ) ;
#121586=FILL_AREA_STYLE ('',( #123733 ) ) ;
#121695=SURFACE_STYLE_FILL_AREA ( #173593 ) ;
#122120=CIRCLE ( 'NONE', #14858, 6.200000000000000178 ) ;
#122925=ORIENTED_EDGE ( 'NONE', *, *, #3337, .T. ) ;
#123733=FILL_AREA_STYLE_COLOUR ( '', #87051 ) ;
#124136=CARTESIAN_POINT ( 'NONE',  ( 0.000000000000000000, -0.4330127018922214077, -6.500000000000000000 ) ) ;
#124768=( GEOMETRIC_REPRESENTATION_CONTEXT ( 3 ) GLOBAL_UNCERTAINTY_ASSIGNED_CONTEXT ( ( #2669 ) ) GLOBAL_UNIT_ASSIGNED_CONTEXT ( ( #201758, #37146, #55541 ) ) REPRESENTATION_CONTEXT ( 'NONE', 'WORKASPACE' ) );
#124946=DIRECTION ( 'NONE',  ( 0.000000000000000000, -1.000000000000000000, 0.000000000000000000 ) ) ;
#125044=CARTESIAN_POINT ( 'NONE',  ( 7.632173801829039911E-16, -0.4330127018922214077, 6.200000000000000178 ) ) ;
#125613=ORIENTED_EDGE ( 'NONE', *, *, #156316, .T. ) ;
#125633=DIRECTION ( 'NONE',  ( 0.000000000000000000, 0.000000000000000000, 1.000000000000000000 ) ) ;
#126049=EDGE_CURVE ( 'NONE', #176746, #23806, #85265, .T. ) ;
#126344=EDGE_LOOP ( 'NONE', ( #93972, #107875, #188219, #95645, #60436 ) ) ;
#129012=DIRECTION ( 'NONE',  ( -0.6929666359396602360, 0.000000000000000000, 0.7209696536432518288 ) ) ;
#129384=TOROIDAL_SURFACE ( 'NONE', #201917, 6.500000000000000000, 0.2999999999999999889 ) ;
#129487=CARTESIAN_POINT ( 'NONE',  ( 0.000000000000000000, -0.4330127018922214077, 0.000000000000000000 ) ) ;
#129965=EDGE_CURVE ( 'NONE', #49964, #23806, #66114, .T. ) ;
#130050=VERTEX_POINT ( 'NONE', #67186 ) ;
#130654=PRODUCT_DEFINITION_CONTEXT ( 'detailed design', #58896, 'design' ) ;
#131115=ORIENTED_EDGE ( 'NONE', *, *, #3337, .F. ) ;
#132002=DIRECTION ( 'NONE',  ( 0.000000000000000000, 0.000000000000000000, 1.000000000000000000 ) ) ;
#134937=PRODUCT_CONTEXT ( 'NONE', #97515, 'mechanical' ) ;
#136941=CARTESIAN_POINT ( 'NONE',  ( -4.296393142825893463, -0.4330127018922214077, 4.470011852588161361 ) ) ;
#137687=CARTESIAN_POINT ( 'NONE',  ( 0.000000000000000000, 0.4330127018922214077, 0.000000000000000000 ) ) ;
#137770=SURFACE_SIDE_STYLE ('',( #21828 ) ) ;
#137874=DIRECTION ( 'NONE',  ( 0.000000000000000000, -1.000000000000000000, 0.000000000000000000 ) ) ;
#138365=VERTEX_POINT ( 'NONE', #68765 ) ;
#139423=CARTESIAN_POINT ( 'NONE',  ( 0.000000000000000000, 0.000000000000000000, 7.049999999999999822 ) ) ;
#139599=CIRCLE ( 'NONE', #156907, 6.200000000000000178 ) ;
#140408=ORIENTED_EDGE ( 'NONE', *, *, #21416, .T. ) ;
#140772=CARTESIAN_POINT ( 'NONE',  ( 0.000000000000000000, -0.6185895741317448682, 0.000000000000000000 ) ) ;
#143089=CARTESIAN_POINT ( 'NONE',  ( 0.000000000000000000, -2.000000000000001776, 0.000000000000000000 ) ) ;
#143384=ORIENTED_EDGE ( 'NONE', *, *, #101370, .T. ) ;
#143667=CIRCLE ( 'NONE', #70906, 0.2999999999999999334 ) ;
#146337=DIRECTION ( 'NONE',  ( 0.000000000000000000, 0.000000000000000000, 1.000000000000000000 ) ) ;
#146437=CIRCLE ( 'NONE', #98035, 1.000000000000000000 ) ;
#147496=DIRECTION ( 'NONE',  ( -1.224646799147353207E-16, 0.000000000000000000, -1.000000000000000000 ) ) ;
#151677=DIRECTION ( 'NONE',  ( 0.000000000000000000, 1.000000000000000000, 0.000000000000000000 ) ) ;
#151814=CARTESIAN_POINT ( 'NONE',  ( 7.671537448944488015E-16, 0.6185895741317448682, -6.264285714285709794 ) ) ;
#152561=TOROIDAL_SURFACE ( 'NONE', #180256, 7.049999999999999822, 0.9999999999999997780 ) ;
#155018=AXIS2_PLACEMENT_3D ( 'NONE', #75175, #109876, #42700 ) ;
#155182=( NAMED_UNIT ( * ) SI_UNIT ( $, .STERADIAN. ) SOLID_ANGLE_UNIT ( ) );
#155448=CIRCLE ( 'NONE', #165804, 6.200000000000000178 ) ;
#156316=EDGE_CURVE ( 'NONE', #171070, #56380, #188314, .T. ) ;
#156907=AXIS2_PLACEMENT_3D ( 'NONE', #85907, #137874, #200692 ) ;
#156926=CARTESIAN_POINT ( 'NONE',  ( 0.000000000000000000, 0.4330127018922214077, 0.000000000000000000 ) ) ;
#157467=ORIENTED_EDGE ( 'NONE', *, *, #32785, .T. ) ;
#157772=PRODUCT ( 'rubber for drip tip', 'rubber for drip tip', '', ( #134937 ) ) ;
#161266=DIRECTION ( 'NONE',  ( 1.000000000000000000, 0.000000000000000000, 0.000000000000000000 ) ) ;
#161483=FACE_OUTER_BOUND ( 'NONE', #41063, .T. ) ;
#163645=CIRCLE ( 'NONE', #191279, 6.264285714285709794 ) ;
#165804=AXIS2_PLACEMENT_3D ( 'NONE', #167915, #151677, #68252 ) ;
#166857=CARTESIAN_POINT ( 'NONE',  ( 4.296393142825894351, -2.000000000000001776, -4.470011852588160473 ) ) ;
#166984=FACE_OUTER_BOUND ( 'NONE', #126344, .T. ) ;
#167773=MANIFOLD_SOLID_BREP ( 'Fillet1', #178179 ) ;
#167915=CARTESIAN_POINT ( 'NONE',  ( 0.000000000000000000, 0.4330127018922214077, 0.000000000000000000 ) ) ;
#168293=LINE ( 'NONE', #186663, #77233 ) ;
#169287=PRESENTATION_STYLE_ASSIGNMENT (( #172504 ) ) ;
#170019=AXIS2_PLACEMENT_3D ( 'NONE', #124136, #56908, #186895 ) ;
#171070=VERTEX_POINT ( 'NONE', #136941 ) ;
#172504=SURFACE_STYLE_USAGE ( .BOTH. , #56612 ) ;
#173002=ORIENTED_EDGE ( 'NONE', *, *, #65071, .T. ) ;
#173573=PRODUCT_DEFINITION ( 'UNKNOWN', '', #107729, #130654 ) ;
#173593=FILL_AREA_STYLE ('',( #104298 ) ) ;
#173595=DIRECTION ( 'NONE',  ( 0.000000000000000000, 1.000000000000000000, 0.000000000000000000 ) ) ;
#175126=DIRECTION ( 'NONE',  ( 0.000000000000000000, 0.000000000000000000, 1.000000000000000000 ) ) ;
#176746=VERTEX_POINT ( 'NONE', #192081 ) ;
#177310=AXIS2_PLACEMENT_3D ( 'NONE', #143089, #64970, #129012 ) ;
#177618=ADVANCED_FACE ( 'NONE', ( #202762 ), #90914, .T. ) ;
#178179=CLOSED_SHELL ( 'NONE', ( #69786, #69800, #79500, #177618, #85539, #212878, #81445, #33425 ) ) ;
#178413=EDGE_CURVE ( 'NONE', #33049, #112763, #146437, .T. ) ;
#178795=CARTESIAN_POINT ( 'NONE',  ( 0.000000000000000000, 0.4330127018922214077, 0.000000000000000000 ) ) ;
#179989=CARTESIAN_POINT ( 'NONE',  ( 7.960204194457795477E-16, -0.4330127018922214077, 6.500000000000000000 ) ) ;
#180142=EDGE_CURVE ( 'NONE', #33049, #138365, #43139, .T. ) ;
#180256=AXIS2_PLACEMENT_3D ( 'NONE', #40378, #173595, #104300 ) ;
#180547=CIRCLE ( 'NONE', #170019, 0.2999999999999999334 ) ;
#181761=ADVANCED_BREP_SHAPE_REPRESENTATION ( '', ( #167773, #200407 ), #124768 ) ;
#181980=EDGE_CURVE ( 'NONE', #49964, #95100, #139599, .T. ) ;
#186663=CARTESIAN_POINT ( 'NONE',  ( -4.296393142825893463, -2.000000000000001776, 4.470011852588161361 ) ) ;
#186895=DIRECTION ( 'NONE',  ( 0.000000000000000000, 0.000000000000000000, 1.000000000000000000 ) ) ;
#187793=AXIS2_PLACEMENT_3D ( 'NONE', #129487, #213804, #195469 ) ;
#188219=ORIENTED_EDGE ( 'NONE', *, *, #91556, .T. ) ;
#188314=CIRCLE ( 'NONE', #29241, 6.200000000000000178 ) ;
#188424=AXIS2_PLACEMENT_3D ( 'NONE', #47772, #67150, #146337 ) ;
#189033=ORIENTED_EDGE ( 'NONE', *, *, #64698, .T. ) ;
#189799=( NAMED_UNIT ( * ) PLANE_ANGLE_UNIT ( ) SI_UNIT ( $, .RADIAN. ) );
#189819=CIRCLE ( 'NONE', #34115, 0.2999999999999999334 ) ;
#190802=ORIENTED_EDGE ( 'NONE', *, *, #181980, .F. ) ;
#190804=ORIENTED_EDGE ( 'NONE', *, *, #55359, .T. ) ;
#191279=AXIS2_PLACEMENT_3D ( 'NONE', #666, #118783, #67800 ) ;
#192081=CARTESIAN_POINT ( 'NONE',  ( 0.000000000000000000, 0.4330127018922214077, 6.200000000000000178 ) ) ;
#193035=CIRCLE ( 'NONE', #155018, 6.200000000000000178 ) ;
#193321=FACE_OUTER_BOUND ( 'NONE', #32954, .T. ) ;
#194748=TOROIDAL_SURFACE ( 'NONE', #187793, 6.500000000000000000, 0.2999999999999999889 ) ;
#195008=TOROIDAL_SURFACE ( 'NONE', #8222, 6.500000000000000000, 0.2999999999999999889 ) ;
#195041=ORIENTED_EDGE ( 'NONE', *, *, #60090, .F. ) ;
#195469=DIRECTION ( 'NONE',  ( 0.000000000000000000, 0.000000000000000000, -1.000000000000000000 ) ) ;
#195963=DIRECTION ( 'NONE',  ( 1.000000000000000000, -0.000000000000000000, 1.224646799147353207E-16 ) ) ;
#196687=TOROIDAL_SURFACE ( 'NONE', #92967, 6.500000000000000000, 0.2999999999999999889 ) ;
#197268=ORIENTED_EDGE ( 'NONE', *, *, #116150, .T. ) ;
#199319=CARTESIAN_POINT ( 'NONE',  ( 0.000000000000000000, -0.4330127018922214077, 0.000000000000000000 ) ) ;
#200407=AXIS2_PLACEMENT_3D ( 'NONE', #95216, #132002, #161266 ) ;
#200513=DIRECTION ( 'NONE',  ( 0.000000000000000000, 0.000000000000000000, 1.000000000000000000 ) ) ;
#200692=DIRECTION ( 'NONE',  ( 0.000000000000000000, 0.000000000000000000, -1.000000000000000000 ) ) ;
#201758=( LENGTH_UNIT ( ) NAMED_UNIT ( * ) SI_UNIT ( .MILLI., .METRE. ) );
#201917=AXIS2_PLACEMENT_3D ( 'NONE', #12000, #61832, #78075 ) ;
#202507=ORIENTED_EDGE ( 'NONE', *, *, #65071, .F. ) ;
#202762=FACE_OUTER_BOUND ( 'NONE', #26764, .T. ) ;
#202827=( LENGTH_UNIT ( ) NAMED_UNIT ( * ) SI_UNIT ( .MILLI., .METRE. ) );
#203560=EDGE_CURVE ( 'NONE', #138365, #33049, #213877, .T. ) ;
#205943=PRESENTATION_STYLE_ASSIGNMENT (( #87936 ) ) ;
#206048=FACE_OUTER_BOUND ( 'NONE', #92398, .T. ) ;
#206714=DIRECTION ( 'NONE',  ( 0.000000000000000000, 1.000000000000000000, 0.000000000000000000 ) ) ;
#206825=CARTESIAN_POINT ( 'NONE',  ( 7.960204194457795477E-16, 0.4330127018922214077, -6.500000000000000000 ) ) ;
#207045=DIRECTION ( 'NONE',  ( 0.000000000000000000, 1.000000000000000000, 0.000000000000000000 ) ) ;
#207850=DIRECTION ( 'NONE',  ( 0.000000000000000000, 1.000000000000000000, 0.000000000000000000 ) ) ;
#207890=DIRECTION ( 'NONE',  ( 1.000000000000000000, -0.000000000000000000, 1.224646799147353207E-16 ) ) ;
#208213=ORIENTED_EDGE ( 'NONE', *, *, #75497, .F. ) ;
#209704=DIRECTION ( 'NONE',  ( -0.6929666359396602360, 0.000000000000000000, 0.7209696536432518288 ) ) ;
#210196=DIRECTION ( 'NONE',  ( 0.000000000000000000, 0.000000000000000000, 1.000000000000000000 ) ) ;
#211224=CYLINDRICAL_SURFACE ( 'NONE', #177310, 6.200000000000000178 ) ;
#211840=FACE_OUTER_BOUND ( 'NONE', #62470, .T. ) ;
#212878=ADVANCED_FACE ( 'NONE', ( #211840 ), #79719, .F. ) ;
#213382=FACE_OUTER_BOUND ( 'NONE', #29872, .T. ) ;
#213804=DIRECTION ( 'NONE',  ( 0.000000000000000000, -1.000000000000000000, 0.000000000000000000 ) ) ;
#213877=CIRCLE ( 'NONE', #47900, 6.264285714285709794 ) ;
#214139=EDGE_CURVE ( 'NONE', #130050, #176746, #155448, .T. ) ;
ENDSEC;
END-ISO-10303-21;
